ISO-10303-21;
HEADER;
FILE_DESCRIPTION (('STEP AP214'),
    '1' );
FILE_NAME ('o-rings series a_iso_O-ring 45x2.65-A-ISO 3601-1.step',
    '2026-10-24T15:06:47',
    ( '' ),
    ( '' ),
    'SwSTEP 2.0',
    'SolidWorks 2026',
    '' );
FILE_SCHEMA (( 'AUTOMOTIVE_DESIGN' ));
ENDSEC;

DATA;
#1=PRODUCT_DEFINITION_SHAPE ( 'NONE', 'NONE',  #7805 ) ;
#5=ORIENTED_EDGE ( 'NONE', *, *, #2695, .F. ) ;
#153=DIRECTION ( 'NONE',  ( -0.000000000000000000, -0.000000000000000000, -1.000000000000000000 ) ) ;
#229=VERTEX_POINT ( 'NONE', #4281 ) ;
#284=COLOUR_RGB ( '',1.000000000000000000, 0.9490196078431372140, 0.9098039215686274384 ) ;
#302=DIRECTION ( 'NONE',  ( -0.000000000000000000, -0.000000000000000000, -1.000000000000000000 ) ) ;
#317=CARTESIAN_POINT ( 'NONE',  ( 0.000000000000000000, 0.000000000000000000, 0.000000000000000000 ) ) ;
#451=APPLICATION_CONTEXT ( 'automotive_design' ) ;
#453=STYLED_ITEM ( 'NONE', ( #5717 ), #1639 ) ;
#459=( LENGTH_UNIT ( ) NAMED_UNIT ( * ) SI_UNIT ( .MILLI., .METRE. ) );
#500=EDGE_CURVE ( 'NONE', #7437, #3613, #793, .T. ) ;
#613=DIRECTION ( 'NONE',  ( -0.000000000000000000, -0.000000000000000000, -1.000000000000000000 ) ) ;
#668=PRODUCT ( 'o-rings series a_iso_O-ring 45x2.65-A-ISO 3601-1', 'o-rings series a_iso_O-ring 45x2.65-A-ISO 3601-1', '', ( #10156 ) ) ;
#766=AXIS2_PLACEMENT_3D ( 'NONE', #7049, #613, #10257 ) ;
#793=CIRCLE ( 'NONE', #3298, 1.324999999999999734 ) ;
#1047=DIRECTION ( 'NONE',  ( -0.000000000000000000, -0.000000000000000000, -1.000000000000000000 ) ) ;
#1086=( NAMED_UNIT ( * ) SI_UNIT ( $, .STERADIAN. ) SOLID_ANGLE_UNIT ( ) );
#1110=EDGE_LOOP ( 'NONE', ( #9799, #7722, #1954, #9276 ) ) ;
#1207=ORIENTED_EDGE ( 'NONE', *, *, #500, .T. ) ;
#1298=TOROIDAL_SURFACE ( 'NONE', #7156, 23.82500000000000284, 1.324999999999999956 ) ;
#1465=EDGE_CURVE ( 'NONE', #229, #7437, #3535, .T. ) ;
#1639=ADVANCED_BREP_SHAPE_REPRESENTATION ( '', ( #3102, #5055 ), #3636 ) ;
#1652=EDGE_LOOP ( 'NONE', ( #6054, #6847, #8487, #1948 ) ) ;
#1774=AXIS2_PLACEMENT_3D ( 'NONE', #2910, #8507, #3030 ) ;
#1780=CLOSED_SHELL ( 'NONE', ( #7325, #8365, #5184, #7203 ) ) ;
#1818=SHAPE_REPRESENTATION_RELATIONSHIP ( 'NONE' , 'NONE' ,  #5114, #1639 ) ;
#1867=( NAMED_UNIT ( * ) PLANE_ANGLE_UNIT ( ) SI_UNIT ( $, .RADIAN. ) );
#1870=MECHANICAL_DESIGN_GEOMETRIC_PRESENTATION_REPRESENTATION('',(#9415),#8052);
#1891=EDGE_CURVE ( 'NONE', #3613, #7437, #3709, .T. ) ;
#1920=SURFACE_STYLE_USAGE ( .BOTH. , #4236 ) ;
#1948=ORIENTED_EDGE ( 'NONE', *, *, #5357, .T. ) ;
#1954=ORIENTED_EDGE ( 'NONE', *, *, #1891, .T. ) ;
#1980=DIRECTION ( 'NONE',  ( -0.000000000000000000, -0.000000000000000000, -1.000000000000000000 ) ) ;
#2011=DIRECTION ( 'NONE',  ( -0.000000000000000000, -0.000000000000000000, -1.000000000000000000 ) ) ;
#2058=ORIENTED_EDGE ( 'NONE', *, *, #1465, .T. ) ;
#2189=CARTESIAN_POINT ( 'NONE',  ( 0.000000000000000000, 0.000000000000000000, 0.000000000000000000 ) ) ;
#2525=FILL_AREA_STYLE ('',( #8312 ) ) ;
#2629=DIRECTION ( 'NONE',  ( -1.000000000000000000, 0.000000000000000000, 0.000000000000000000 ) ) ;
#2695=EDGE_CURVE ( 'NONE', #7425, #3613, #3069, .T. ) ;
#2910=CARTESIAN_POINT ( 'NONE',  ( 0.000000000000000000, 0.000000000000000000, 0.000000000000000000 ) ) ;
#2917=CIRCLE ( 'NONE', #5075, 25.15000000000000213 ) ;
#2971=FACE_OUTER_BOUND ( 'NONE', #1110, .T. ) ;
#2996=PRODUCT_DEFINITION_CONTEXT ( 'detailed design', #451, 'design' ) ;
#3030=DIRECTION ( 'NONE',  ( -1.000000000000000000, 0.000000000000000000, 0.000000000000000000 ) ) ;
#3069=CIRCLE ( 'NONE', #10254, 25.15000000000000213 ) ;
#3102=MANIFOLD_SOLID_BREP ( 'Sweep1', #1780 ) ;
#3148=MECHANICAL_DESIGN_GEOMETRIC_PRESENTATION_REPRESENTATION('',(#453),#7146);
#3200=CARTESIAN_POINT ( 'NONE',  ( 0.000000000000000000, 0.000000000000000000, 0.000000000000000000 ) ) ;
#3243=ORIENTED_EDGE ( 'NONE', *, *, #5357, .F. ) ;
#3266=ORIENTED_EDGE ( 'NONE', *, *, #7879, .T. ) ;
#3298=AXIS2_PLACEMENT_3D ( 'NONE', #7909, #7962, #9582 ) ;
#3418=DIRECTION ( 'NONE',  ( -1.224646799147353207E-16, 1.000000000000000000, 0.000000000000000000 ) ) ;
#3445=( NAMED_UNIT ( * ) SI_UNIT ( $, .STERADIAN. ) SOLID_ANGLE_UNIT ( ) );
#3493=DIRECTION ( 'NONE',  ( 0.000000000000000000, -1.000000000000000000, 0.000000000000000000 ) ) ;
#3521=APPLICATION_CONTEXT ( 'automotive_design' ) ;
#3535=CIRCLE ( 'NONE', #6036, 22.50000000000000355 ) ;
#3542=FACE_OUTER_BOUND ( 'NONE', #1652, .T. ) ;
#3613=VERTEX_POINT ( 'NONE', #9407 ) ;
#3636=( GEOMETRIC_REPRESENTATION_CONTEXT ( 3 ) GLOBAL_UNCERTAINTY_ASSIGNED_CONTEXT ( ( #6959 ) ) GLOBAL_UNIT_ASSIGNED_CONTEXT ( ( #9686, #1867, #3445 ) ) REPRESENTATION_CONTEXT ( 'NONE', 'WORKASPACE' ) );
#3709=CIRCLE ( 'NONE', #9402, 1.324999999999999734 ) ;
#3862=DIRECTION ( 'NONE',  ( 0.000000000000000000, -1.000000000000000000, 0.000000000000000000 ) ) ;
#3998=CIRCLE ( 'NONE', #9801, 1.324999999999999956 ) ;
#4033=UNCERTAINTY_MEASURE_WITH_UNIT (LENGTH_MEASURE( 1.000000000000000082E-05 ), #5013, 'distance_accuracy_value', 'NONE');
#4045=EDGE_CURVE ( 'NONE', #3613, #7425, #2917, .T. ) ;
#4051=DIRECTION ( 'NONE',  ( 0.000000000000000000, 0.000000000000000000, -1.000000000000000000 ) ) ;
#4154=DIRECTION ( 'NONE',  ( 0.000000000000000000, 0.000000000000000000, 1.000000000000000000 ) ) ;
#4236=SURFACE_SIDE_STYLE ('',( #5854 ) ) ;
#4281=CARTESIAN_POINT ( 'NONE',  ( -22.50000000000000355, 0.000000000000000000, 1.622657008870243228E-16 ) ) ;
#4288=CARTESIAN_POINT ( 'NONE',  ( 0.000000000000000000, 0.000000000000000000, 1.622657008870242981E-16 ) ) ;
#4331=CARTESIAN_POINT ( 'NONE',  ( -23.82500000000000284, 0.000000000000000000, 0.000000000000000000 ) ) ;
#4444=UNCERTAINTY_MEASURE_WITH_UNIT (LENGTH_MEASURE( 1.000000000000000082E-05 ), #459, 'distance_accuracy_value', 'NONE');
#4469=TOROIDAL_SURFACE ( 'NONE', #9159, 23.82500000000000284, 1.324999999999999956 ) ;
#4482=DIRECTION ( 'NONE',  ( 0.000000000000000000, 0.000000000000000000, -1.000000000000000000 ) ) ;
#4769=AXIS2_PLACEMENT_3D ( 'NONE', #3200, #153, #7262 ) ;
#4813=FACE_OUTER_BOUND ( 'NONE', #5212, .T. ) ;
#4992=CARTESIAN_POINT ( 'NONE',  ( 23.82500000000000284, 2.917720998968569322E-15, 0.000000000000000000 ) ) ;
#5013=( LENGTH_UNIT ( ) NAMED_UNIT ( * ) SI_UNIT ( .MILLI., .METRE. ) );
#5055=AXIS2_PLACEMENT_3D ( 'NONE', #9842, #4154, #9744 ) ;
#5075=AXIS2_PLACEMENT_3D ( 'NONE', #8330, #9952, #2629 ) ;
#5114=SHAPE_REPRESENTATION ( 'o-rings series a_iso_O-ring 45x2.65-A-ISO 3601-1', ( #5055 ), #3636 ) ;
#5184=ADVANCED_FACE ( 'NONE', ( #4813 ), #6281, .T. ) ;
#5212=EDGE_LOOP ( 'NONE', ( #5, #3243, #2058, #1207 ) ) ;
#5357=EDGE_CURVE ( 'NONE', #229, #7425, #8271, .T. ) ;
#5432=EDGE_CURVE ( 'NONE', #7437, #229, #9764, .T. ) ;
#5717=PRESENTATION_STYLE_ASSIGNMENT (( #1920 ) ) ;
#5854=SURFACE_STYLE_FILL_AREA ( #2525 ) ;
#5927=AXIS2_PLACEMENT_3D ( 'NONE', #8406, #3862, #4482 ) ;
#5934=ORIENTED_EDGE ( 'NONE', *, *, #5432, .F. ) ;
#6036=AXIS2_PLACEMENT_3D ( 'NONE', #4288, #1047, #6639 ) ;
#6054=ORIENTED_EDGE ( 'NONE', *, *, #4045, .F. ) ;
#6281=TOROIDAL_SURFACE ( 'NONE', #4769, 23.82500000000000284, 1.324999999999999956 ) ;
#6639=DIRECTION ( 'NONE',  ( -1.000000000000000000, 0.000000000000000000, 0.000000000000000000 ) ) ;
#6731=CARTESIAN_POINT ( 'NONE',  ( 0.000000000000000000, 0.000000000000000000, 0.000000000000000000 ) ) ;
#6847=ORIENTED_EDGE ( 'NONE', *, *, #500, .F. ) ;
#6959=UNCERTAINTY_MEASURE_WITH_UNIT (LENGTH_MEASURE( 1.000000000000000082E-05 ), #9686, 'distance_accuracy_value', 'NONE');
#6984=PRODUCT_DEFINITION_FORMATION_WITH_SPECIFIED_SOURCE ( 'ANY', '', #668, .NOT_KNOWN. ) ;
#7049=CARTESIAN_POINT ( 'NONE',  ( 0.000000000000000000, 0.000000000000000000, 1.622657008870242981E-16 ) ) ;
#7146=( GEOMETRIC_REPRESENTATION_CONTEXT ( 3 ) GLOBAL_UNCERTAINTY_ASSIGNED_CONTEXT ( ( #4033 ) ) GLOBAL_UNIT_ASSIGNED_CONTEXT ( ( #5013, #8999, #8263 ) ) REPRESENTATION_CONTEXT ( 'NONE', 'WORKASPACE' ) );
#7156=AXIS2_PLACEMENT_3D ( 'NONE', #2189, #2011, #8522 ) ;
#7203=ADVANCED_FACE ( 'NONE', ( #3542 ), #4469, .T. ) ;
#7262=DIRECTION ( 'NONE',  ( -1.000000000000000000, 0.000000000000000000, 0.000000000000000000 ) ) ;
#7325=ADVANCED_FACE ( 'NONE', ( #7617 ), #1298, .T. ) ;
#7409=( NAMED_UNIT ( * ) PLANE_ANGLE_UNIT ( ) SI_UNIT ( $, .RADIAN. ) );
#7425=VERTEX_POINT ( 'NONE', #7894 ) ;
#7437=VERTEX_POINT ( 'NONE', #8835 ) ;
#7454=TOROIDAL_SURFACE ( 'NONE', #1774, 23.82500000000000284, 1.324999999999999956 ) ;
#7477=DIRECTION ( 'NONE',  ( -1.000000000000000000, 0.000000000000000000, 0.000000000000000000 ) ) ;
#7617=FACE_OUTER_BOUND ( 'NONE', #8557, .T. ) ;
#7722=ORIENTED_EDGE ( 'NONE', *, *, #2695, .T. ) ;
#7805=PRODUCT_DEFINITION ( 'UNKNOWN', '', #6984, #2996 ) ;
#7879=EDGE_CURVE ( 'NONE', #7425, #229, #3998, .T. ) ;
#7894=CARTESIAN_POINT ( 'NONE',  ( -25.15000000000000213, 0.000000000000000000, 0.000000000000000000 ) ) ;
#7909=CARTESIAN_POINT ( 'NONE',  ( 23.82500000000000284, 2.917720998968569322E-15, 0.000000000000000000 ) ) ;
#7962=DIRECTION ( 'NONE',  ( -1.224646799147353207E-16, 1.000000000000000000, 0.000000000000000000 ) ) ;
#8052=( GEOMETRIC_REPRESENTATION_CONTEXT ( 3 ) GLOBAL_UNCERTAINTY_ASSIGNED_CONTEXT ( ( #4444 ) ) GLOBAL_UNIT_ASSIGNED_CONTEXT ( ( #459, #7409, #1086 ) ) REPRESENTATION_CONTEXT ( 'NONE', 'WORKASPACE' ) );
#8263=( NAMED_UNIT ( * ) SI_UNIT ( $, .STERADIAN. ) SOLID_ANGLE_UNIT ( ) );
#8271=CIRCLE ( 'NONE', #5927, 1.324999999999999956 ) ;
#8312=FILL_AREA_STYLE_COLOUR ( '', #284 ) ;
#8330=CARTESIAN_POINT ( 'NONE',  ( 0.000000000000000000, 0.000000000000000000, 0.000000000000000000 ) ) ;
#8365=ADVANCED_FACE ( 'NONE', ( #2971 ), #7454, .T. ) ;
#8366=SHAPE_DEFINITION_REPRESENTATION ( #1, #5114 ) ;
#8406=CARTESIAN_POINT ( 'NONE',  ( -23.82500000000000284, 0.000000000000000000, 0.000000000000000000 ) ) ;
#8487=ORIENTED_EDGE ( 'NONE', *, *, #5432, .T. ) ;
#8507=DIRECTION ( 'NONE',  ( -0.000000000000000000, -0.000000000000000000, -1.000000000000000000 ) ) ;
#8522=DIRECTION ( 'NONE',  ( -1.000000000000000000, 0.000000000000000000, 0.000000000000000000 ) ) ;
#8557=EDGE_LOOP ( 'NONE', ( #10169, #10082, #3266, #5934 ) ) ;
#8835=CARTESIAN_POINT ( 'NONE',  ( 22.50000000000000355, 2.755455298081545172E-15, 0.000000000000000000 ) ) ;
#8999=( NAMED_UNIT ( * ) PLANE_ANGLE_UNIT ( ) SI_UNIT ( $, .RADIAN. ) );
#9159=AXIS2_PLACEMENT_3D ( 'NONE', #6731, #302, #9872 ) ;
#9276=ORIENTED_EDGE ( 'NONE', *, *, #1465, .F. ) ;
#9402=AXIS2_PLACEMENT_3D ( 'NONE', #4992, #3418, #9907 ) ;
#9407=CARTESIAN_POINT ( 'NONE',  ( 25.15000000000000213, 3.079986699855593473E-15, 0.000000000000000000 ) ) ;
#9415=STYLED_ITEM('',(#10408),#3102);
#9582=DIRECTION ( 'NONE',  ( -1.000000000000000000, -1.224646799147352961E-16, 0.000000000000000000 ) ) ;
#9686=( LENGTH_UNIT ( ) NAMED_UNIT ( * ) SI_UNIT ( .MILLI., .METRE. ) );
#9744=DIRECTION ( 'NONE',  ( 1.000000000000000000, 0.000000000000000000, 0.000000000000000000 ) ) ;
#9764=CIRCLE ( 'NONE', #766, 22.50000000000000355 ) ;
#9799=ORIENTED_EDGE ( 'NONE', *, *, #7879, .F. ) ;
#9801=AXIS2_PLACEMENT_3D ( 'NONE', #4331, #3493, #4051 ) ;
#9842=CARTESIAN_POINT ( 'NONE',  ( 0.000000000000000000, 0.000000000000000000, 0.000000000000000000 ) ) ;
#9872=DIRECTION ( 'NONE',  ( -1.000000000000000000, 0.000000000000000000, 0.000000000000000000 ) ) ;
#9907=DIRECTION ( 'NONE',  ( -1.000000000000000000, -1.224646799147352961E-16, 0.000000000000000000 ) ) ;
#9952=DIRECTION ( 'NONE',  ( -0.000000000000000000, -0.000000000000000000, -1.000000000000000000 ) ) ;
#10082=ORIENTED_EDGE ( 'NONE', *, *, #4045, .T. ) ;
#10156=PRODUCT_CONTEXT ( 'NONE', #3521, 'mechanical' ) ;
#10169=ORIENTED_EDGE ( 'NONE', *, *, #1891, .F. ) ;
#10254=AXIS2_PLACEMENT_3D ( 'NONE', #317, #1980, #7477 ) ;
#10257=DIRECTION ( 'NONE',  ( -1.000000000000000000, 0.000000000000000000, 0.000000000000000000 ) ) ;
#10402=COLOUR_RGB('Black',0.12,0.14,0.17);
#10403=FILL_AREA_STYLE_COLOUR('',#10402);
#10404=FILL_AREA_STYLE('',(#10403));
#10405=SURFACE_STYLE_FILL_AREA(#10404);
#10406=SURFACE_SIDE_STYLE('',(#10405));
#10407=SURFACE_STYLE_USAGE(.BOTH.,#10406);
#10408=PRESENTATION_STYLE_ASSIGNMENT((#10407));
ENDSEC;
END-ISO-10303-21;
